ISO-10303-21;
HEADER;
/* Generated by software containing ST-Developer
 * from STEP Tools, Inc. (www.steptools.com) 
 */

FILE_DESCRIPTION(
/* description */ ('', 'CAx-IF Rec.Pracs.---Representation and Presentation of Product Manufa
cturing Information (PMI)---4.0---2014-10-13'),
/* implementation_level */ '2;1');

FILE_NAME(
/* name */ 'Flat Washer M8.step',
/* time_stamp */ '2026-10-28T14:45:12+01:00',
/* author */ (''),
/* organization */ (''),
/* preprocessor_version */ 'ST-DEVELOPER v20.2',
/* originating_system */ 'Autodesk Translation Framework v15.17.0.0',
/* authorisation */ '');

FILE_SCHEMA (('AP242_MANAGED_MODEL_BASED_3D_ENGINEERING_MIM_LF { 1 0 10303 442 2 1 4 }'));
ENDSEC;

DATA;
#10=MECHANICAL_DESIGN_GEOMETRIC_PRESENTATION_REPRESENTATION('',(#266),#52164);
#230=TOROIDAL_SURFACE('',#10140,6.2,0.8);
#240=SHAPE_REPRESENTATION_RELATIONSHIP('SRR','None',#52219,#253);
#253=ADVANCED_BREP_SHAPE_REPRESENTATION('',(#279),#52159);
#266=STYLED_ITEM('',(#52325),#279);
#279=MANIFOLD_SOLID_BREP('Body1',#9126);
#315=FACE_BOUND('',#1578,.T.);
#316=FACE_BOUND('',#1581,.T.);
#503=PLANE('',#10133);
#504=PLANE('',#10138);
#1013=FACE_OUTER_BOUND('',#1577,.T.);
#1014=FACE_OUTER_BOUND('',#1579,.T.);
#1015=FACE_OUTER_BOUND('',#1580,.T.);
#1016=FACE_OUTER_BOUND('',#1582,.T.);
#1577=EDGE_LOOP('',(#8158));
#1578=EDGE_LOOP('',(#8159));
#1579=EDGE_LOOP('',(#8160,#8161,#8162,#8163));
#1580=EDGE_LOOP('',(#8164));
#1581=EDGE_LOOP('',(#8165));
#1582=EDGE_LOOP('',(#8166,#8167,#8168,#8169));
#2066=CIRCLE('',#10134,6.2);
#2067=CIRCLE('',#10135,4.);
#2068=CIRCLE('',#10137,4.);
#2069=CIRCLE('',#10139,6.2);
#2070=CIRCLE('',#10141,0.8);
#2895=LINE('',#46055,#3360);
#3360=VECTOR('',#12367,4.);
#4193=VERTEX_POINT('',#46049);
#4194=VERTEX_POINT('',#46051);
#4195=VERTEX_POINT('',#46054);
#4196=VERTEX_POINT('',#46058);
#5525=EDGE_CURVE('',#4193,#4193,#2066,.T.);
#5526=EDGE_CURVE('',#4194,#4194,#2067,.T.);
#5527=EDGE_CURVE('',#4194,#4195,#2895,.T.);
#5528=EDGE_CURVE('',#4195,#4195,#2068,.T.);
#5529=EDGE_CURVE('',#4196,#4196,#2069,.T.);
#5530=EDGE_CURVE('',#4196,#4193,#2070,.T.);
#8158=ORIENTED_EDGE('',*,*,#5525,.T.);
#8159=ORIENTED_EDGE('',*,*,#5526,.F.);
#8160=ORIENTED_EDGE('',*,*,#5526,.T.);
#8161=ORIENTED_EDGE('',*,*,#5527,.T.);
#8162=ORIENTED_EDGE('',*,*,#5528,.F.);
#8163=ORIENTED_EDGE('',*,*,#5527,.F.);
#8164=ORIENTED_EDGE('',*,*,#5529,.T.);
#8165=ORIENTED_EDGE('',*,*,#5528,.T.);
#8166=ORIENTED_EDGE('',*,*,#5529,.F.);
#8167=ORIENTED_EDGE('',*,*,#5530,.T.);
#8168=ORIENTED_EDGE('',*,*,#5525,.F.);
#8169=ORIENTED_EDGE('',*,*,#5530,.F.);
#8568=CYLINDRICAL_SURFACE('',#10136,4.);
#9076=ADVANCED_FACE('',(#1013,#315),#503,.F.);
#9077=ADVANCED_FACE('',(#1014),#8568,.F.);
#9078=ADVANCED_FACE('',(#1015,#316),#504,.T.);
#9079=ADVANCED_FACE('',(#1016),#230,.T.);
#9126=CLOSED_SHELL('',(#9076,#9077,#9078,#9079));
#10132=AXIS2_PLACEMENT_3D('',#46047,#12357,#12358);
#10133=AXIS2_PLACEMENT_3D('',#46048,#12359,#12360);
#10134=AXIS2_PLACEMENT_3D('',#46050,#12361,#12362);
#10135=AXIS2_PLACEMENT_3D('',#46052,#12363,#12364);
#10136=AXIS2_PLACEMENT_3D('',#46053,#12365,#12366);
#10137=AXIS2_PLACEMENT_3D('',#46056,#12368,#12369);
#10138=AXIS2_PLACEMENT_3D('',#46057,#12370,#12371);
#10139=AXIS2_PLACEMENT_3D('',#46059,#12372,#12373);
#10140=AXIS2_PLACEMENT_3D('',#46060,#12374,#12375);
#10141=AXIS2_PLACEMENT_3D('',#46061,#12376,#12377);
#12357=DIRECTION('axis',(0.,0.,1.));
#12358=DIRECTION('refdir',(1.,0.,0.));
#12359=DIRECTION('center_axis',(0.,1.,0.));
#12360=DIRECTION('ref_axis',(1.,0.,0.));
#12361=DIRECTION('center_axis',(0.,-1.,0.));
#12362=DIRECTION('ref_axis',(1.,0.,0.));
#12363=DIRECTION('center_axis',(0.,-1.,0.));
#12364=DIRECTION('ref_axis',(1.,0.,0.));
#12365=DIRECTION('center_axis',(0.,1.,0.));
#12366=DIRECTION('ref_axis',(1.,0.,0.));
#12367=DIRECTION('',(0.,1.,0.));
#12368=DIRECTION('center_axis',(0.,-1.,0.));
#12369=DIRECTION('ref_axis',(1.,0.,0.));
#12370=DIRECTION('center_axis',(0.,1.,0.));
#12371=DIRECTION('ref_axis',(1.,0.,0.));
#12372=DIRECTION('center_axis',(0.,1.,0.));
#12373=DIRECTION('ref_axis',(-1.,0.,0.));
#12374=DIRECTION('center_axis',(0.,1.,0.));
#12375=DIRECTION('ref_axis',(-0.999990481172045,0.,-0.0043632058514502));
#12376=DIRECTION('center_axis',(0.00436320585145007,0.,-0.999990481172045));
#12377=DIRECTION('ref_axis',(0.999990481172045,0.,0.00436320585145007));
#46047=CARTESIAN_POINT('',(0.,0.,0.));
#46048=CARTESIAN_POINT('Origin',(0.,0.,0.));
#46049=CARTESIAN_POINT('',(6.19994098326668,0.,0.0270518762789905));
#46050=CARTESIAN_POINT('Origin',(0.,0.,0.));
#46051=CARTESIAN_POINT('',(-4.,0.,4.89858719658941E-16));
#46052=CARTESIAN_POINT('Origin',(0.,0.,0.));
#46053=CARTESIAN_POINT('Origin',(0.,0.,0.));
#46054=CARTESIAN_POINT('',(-4.,1.6,4.89858719658941E-16));
#46055=CARTESIAN_POINT('',(-4.,0.,4.89858719658941E-16));
#46056=CARTESIAN_POINT('Origin',(0.,1.6,0.));
#46057=CARTESIAN_POINT('Origin',(0.,1.6,0.));
#46058=CARTESIAN_POINT('',(6.19994098326668,1.6,0.0270518762789905));
#46059=CARTESIAN_POINT('Origin',(0.,1.6,0.));
#46060=CARTESIAN_POINT('Origin',(0.,0.8,0.));
#46061=CARTESIAN_POINT('Origin',(6.19994098326668,0.8,0.0270518762789905));
#52144=UNCERTAINTY_MEASURE_WITH_UNIT(LENGTH_MEASURE(0.01),#52165,
'DISTANCE_ACCURACY_VALUE',
'Maximum model space distance between geometric entities at asserted c
onnectivities');
#52149=UNCERTAINTY_MEASURE_WITH_UNIT(LENGTH_MEASURE(0.01),#52165,
'DISTANCE_ACCURACY_VALUE',
'Maximum model space distance between geometric entities at asserted c
onnectivities');
#52159=(
GEOMETRIC_REPRESENTATION_CONTEXT(3)
GLOBAL_UNCERTAINTY_ASSIGNED_CONTEXT((#52144))
GLOBAL_UNIT_ASSIGNED_CONTEXT((#52165,#52167,#52168))
REPRESENTATION_CONTEXT('','3D')
);
#52164=(
GEOMETRIC_REPRESENTATION_CONTEXT(3)
GLOBAL_UNCERTAINTY_ASSIGNED_CONTEXT((#52149))
GLOBAL_UNIT_ASSIGNED_CONTEXT((#52165,#52167,#52168))
REPRESENTATION_CONTEXT('','3D')
);
#52165=(
LENGTH_UNIT()
NAMED_UNIT(*)
SI_UNIT(.MILLI.,.METRE.)
);
#52167=(
NAMED_UNIT(*)
PLANE_ANGLE_UNIT()
SI_UNIT($,.RADIAN.)
);
#52168=(
NAMED_UNIT(*)
SI_UNIT($,.STERADIAN.)
SOLID_ANGLE_UNIT()
);
#52178=SHAPE_DEFINITION_REPRESENTATION(#52192,#52219);
#52192=PRODUCT_DEFINITION_SHAPE('',$,#52234);
#52219=SHAPE_REPRESENTATION('',(#10132),#52159);
#52224=PRODUCT_DEFINITION_CONTEXT('part definition',#52268,'design');
#52234=PRODUCT_DEFINITION('Flat Washer M8','Flat Washer M8',#52248,#52224);
#52248=PRODUCT_DEFINITION_FORMATION('',$,#52279);
#52268=APPLICATION_CONTEXT('Managed model based 3d engineering');
#52269=PRODUCT_CONTEXT('part definition',#52268,'mechanical');
#52279=PRODUCT('Flat Washer M8','Flat Washer M8','NOT SPECIFIED',(#52269));
#52319=COLOUR_RGB('Black',0.12,0.14,0.17);
#52320=FILL_AREA_STYLE_COLOUR('',#52319);
#52321=FILL_AREA_STYLE('',(#52320));
#52322=SURFACE_STYLE_FILL_AREA(#52321);
#52323=SURFACE_SIDE_STYLE('',(#52322));
#52324=SURFACE_STYLE_USAGE(.BOTH.,#52323);
#52325=PRESENTATION_STYLE_ASSIGNMENT((#52324));
ENDSEC;
END-ISO-10303-21;
